ISO-10303-21;
HEADER;
/* Generated by software containing ST-Developer
 * from STEP Tools, Inc. (www.steptools.com) 
 */

FILE_DESCRIPTION(
/* description */ ('Counter shaft with two pulleys and keyed hub'),
/* implementation_level */ '2;1');

FILE_NAME(
/* name */ 'Cap Screw - M5x20.step',
/* time_stamp */ '2026-10-27T10:46:10-07:00',
/* author */ (''),
/* organization */ (''),
/* preprocessor_version */ 'ST-DEVELOPER v20.2',
/* originating_system */ 'Autodesk Translation Framework v15.17.0.0',
/* authorisation */ '');

FILE_SCHEMA (('AUTOMOTIVE_DESIGN { 1 0 10303 214 3 1 1 }'));
ENDSEC;

DATA;
#10=MECHANICAL_DESIGN_GEOMETRIC_PRESENTATION_REPRESENTATION('',(#313),#10821);
#14=CONICAL_SURFACE('',#6487,0.4,0.785398163397448);
#15=CONICAL_SURFACE('',#6491,0.41,0.785398163397448);
#16=CONICAL_SURFACE('',#6495,0.26,0.463647609000806);
#17=CONICAL_SURFACE('',#6499,0.225,0.785398163397448);
#21=ORIENTED_CLOSED_SHELL('',*,#5598,.F.);
#23=BREP_WITH_VOIDS('Body1',#5597,(#21));
#262=SHAPE_REPRESENTATION_RELATIONSHIP('SRR','None',#10950,#287);
#287=ADVANCED_BREP_SHAPE_REPRESENTATION('',(#23),#10818);
#313=STYLED_ITEM('',(#11142),#23);
#429=FACE_BOUND('',#1271,.T.);
#558=PLANE('',#6485);
#559=PLANE('',#6493);
#560=PLANE('',#6501);
#561=PLANE('',#6502);
#562=PLANE('',#6503);
#563=PLANE('',#6504);
#564=PLANE('',#6505);
#565=PLANE('',#6506);
#566=PLANE('',#6507);
#567=PLANE('',#6508);
#568=PLANE('',#6509);
#863=FACE_OUTER_BOUND('',#1266,.T.);
#864=FACE_OUTER_BOUND('',#1267,.T.);
#865=FACE_OUTER_BOUND('',#1268,.T.);
#866=FACE_OUTER_BOUND('',#1269,.T.);
#867=FACE_OUTER_BOUND('',#1270,.T.);
#868=FACE_OUTER_BOUND('',#1272,.T.);
#869=FACE_OUTER_BOUND('',#1273,.T.);
#870=FACE_OUTER_BOUND('',#1274,.T.);
#871=FACE_OUTER_BOUND('',#1275,.T.);
#872=FACE_OUTER_BOUND('',#1276,.T.);
#873=FACE_OUTER_BOUND('',#1277,.T.);
#874=FACE_OUTER_BOUND('',#1278,.T.);
#875=FACE_OUTER_BOUND('',#1279,.T.);
#876=FACE_OUTER_BOUND('',#1280,.T.);
#877=FACE_OUTER_BOUND('',#1281,.T.);
#878=FACE_OUTER_BOUND('',#1282,.T.);
#879=FACE_OUTER_BOUND('',#1283,.T.);
#1266=EDGE_LOOP('',(#4951));
#1267=EDGE_LOOP('',(#4952,#4953,#4954,#4955));
#1268=EDGE_LOOP('',(#4956,#4957,#4958,#4959));
#1269=EDGE_LOOP('',(#4960,#4961,#4962,#4963));
#1270=EDGE_LOOP('',(#4964));
#1271=EDGE_LOOP('',(#4965));
#1272=EDGE_LOOP('',(#4966,#4967,#4968,#4969));
#1273=EDGE_LOOP('',(#4970,#4971,#4972,#4973));
#1274=EDGE_LOOP('',(#4974,#4975,#4976,#4977));
#1275=EDGE_LOOP('',(#4978));
#1276=EDGE_LOOP('',(#4979,#4980,#4981,#4982));
#1277=EDGE_LOOP('',(#4983,#4984,#4985,#4986));
#1278=EDGE_LOOP('',(#4987,#4988,#4989,#4990));
#1279=EDGE_LOOP('',(#4991,#4992,#4993,#4994));
#1280=EDGE_LOOP('',(#4995,#4996,#4997,#4998));
#1281=EDGE_LOOP('',(#4999,#5000,#5001,#5002));
#1282=EDGE_LOOP('',(#5003,#5004,#5005,#5006,#5007,#5008));
#1283=EDGE_LOOP('',(#5009,#5010,#5011,#5012,#5013,#5014));
#1627=LINE('',#10573,#2016);
#1628=LINE('',#10577,#2017);
#1629=LINE('',#10581,#2018);
#1630=LINE('',#10588,#2019);
#1631=LINE('',#10592,#2020);
#1632=LINE('',#10596,#2021);
#1633=LINE('',#10601,#2022);
#1634=LINE('',#10603,#2023);
#1635=LINE('',#10605,#2024);
#1636=LINE('',#10606,#2025);
#1637=LINE('',#10609,#2026);
#1638=LINE('',#10611,#2027);
#1639=LINE('',#10612,#2028);
#1640=LINE('',#10615,#2029);
#1641=LINE('',#10617,#2030);
#1642=LINE('',#10618,#2031);
#1643=LINE('',#10621,#2032);
#1644=LINE('',#10623,#2033);
#1645=LINE('',#10624,#2034);
#1646=LINE('',#10627,#2035);
#1647=LINE('',#10629,#2036);
#1648=LINE('',#10630,#2037);
#1649=LINE('',#10632,#2038);
#1650=LINE('',#10633,#2039);
#2016=VECTOR('',#8103,0.4);
#2017=VECTOR('',#8108,0.425);
#2018=VECTOR('',#8113,0.41);
#2019=VECTOR('',#8122,0.26);
#2020=VECTOR('',#8127,0.25);
#2021=VECTOR('',#8132,0.225);
#2022=VECTOR('',#8137,1.);
#2023=VECTOR('',#8138,1.);
#2024=VECTOR('',#8139,1.);
#2025=VECTOR('',#8140,1.);
#2026=VECTOR('',#8143,1.);
#2027=VECTOR('',#8144,1.);
#2028=VECTOR('',#8145,1.);
#2029=VECTOR('',#8148,1.);
#2030=VECTOR('',#8149,1.);
#2031=VECTOR('',#8150,1.);
#2032=VECTOR('',#8153,1.);
#2033=VECTOR('',#8154,1.);
#2034=VECTOR('',#8155,1.);
#2035=VECTOR('',#8158,1.);
#2036=VECTOR('',#8159,1.);
#2037=VECTOR('',#8160,1.);
#2038=VECTOR('',#8163,1.);
#2039=VECTOR('',#8164,1.);
#2372=CIRCLE('',#6486,0.375);
#2373=CIRCLE('',#6488,0.425);
#2374=CIRCLE('',#6490,0.425);
#2375=CIRCLE('',#6492,0.395);
#2376=CIRCLE('',#6494,0.27);
#2377=CIRCLE('',#6496,0.24505);
#2378=CIRCLE('',#6498,0.24505);
#2379=CIRCLE('',#6500,0.2);
#2835=VERTEX_POINT('',#10568);
#2836=VERTEX_POINT('',#10571);
#2837=VERTEX_POINT('',#10575);
#2838=VERTEX_POINT('',#10579);
#2839=VERTEX_POINT('',#10583);
#2840=VERTEX_POINT('',#10586);
#2841=VERTEX_POINT('',#10590);
#2842=VERTEX_POINT('',#10594);
#2843=VERTEX_POINT('',#10599);
#2844=VERTEX_POINT('',#10600);
#2845=VERTEX_POINT('',#10602);
#2846=VERTEX_POINT('',#10604);
#2847=VERTEX_POINT('',#10608);
#2848=VERTEX_POINT('',#10610);
#2849=VERTEX_POINT('',#10614);
#2850=VERTEX_POINT('',#10616);
#2851=VERTEX_POINT('',#10620);
#2852=VERTEX_POINT('',#10622);
#2853=VERTEX_POINT('',#10626);
#2854=VERTEX_POINT('',#10628);
#3548=EDGE_CURVE('',#2835,#2835,#2372,.T.);
#3549=EDGE_CURVE('',#2836,#2836,#2373,.T.);
#3550=EDGE_CURVE('',#2836,#2835,#1627,.T.);
#3551=EDGE_CURVE('',#2837,#2837,#2374,.T.);
#3552=EDGE_CURVE('',#2837,#2836,#1628,.T.);
#3553=EDGE_CURVE('',#2838,#2838,#2375,.T.);
#3554=EDGE_CURVE('',#2838,#2837,#1629,.T.);
#3555=EDGE_CURVE('',#2839,#2839,#2376,.T.);
#3556=EDGE_CURVE('',#2840,#2840,#2377,.F.);
#3557=EDGE_CURVE('',#2840,#2839,#1630,.T.);
#3558=EDGE_CURVE('',#2841,#2841,#2378,.F.);
#3559=EDGE_CURVE('',#2841,#2840,#1631,.T.);
#3560=EDGE_CURVE('',#2842,#2842,#2379,.T.);
#3561=EDGE_CURVE('',#2842,#2841,#1632,.T.);
#3562=EDGE_CURVE('',#2843,#2844,#1633,.T.);
#3563=EDGE_CURVE('',#2844,#2845,#1634,.T.);
#3564=EDGE_CURVE('',#2845,#2846,#1635,.T.);
#3565=EDGE_CURVE('',#2843,#2846,#1636,.T.);
#3566=EDGE_CURVE('',#2844,#2847,#1637,.T.);
#3567=EDGE_CURVE('',#2847,#2848,#1638,.T.);
#3568=EDGE_CURVE('',#2848,#2845,#1639,.T.);
#3569=EDGE_CURVE('',#2847,#2849,#1640,.T.);
#3570=EDGE_CURVE('',#2849,#2850,#1641,.T.);
#3571=EDGE_CURVE('',#2850,#2848,#1642,.T.);
#3572=EDGE_CURVE('',#2849,#2851,#1643,.T.);
#3573=EDGE_CURVE('',#2851,#2852,#1644,.T.);
#3574=EDGE_CURVE('',#2852,#2850,#1645,.T.);
#3575=EDGE_CURVE('',#2851,#2853,#1646,.T.);
#3576=EDGE_CURVE('',#2853,#2854,#1647,.T.);
#3577=EDGE_CURVE('',#2854,#2852,#1648,.T.);
#3578=EDGE_CURVE('',#2853,#2843,#1649,.T.);
#3579=EDGE_CURVE('',#2846,#2854,#1650,.T.);
#4951=ORIENTED_EDGE('',*,*,#3548,.F.);
#4952=ORIENTED_EDGE('',*,*,#3549,.F.);
#4953=ORIENTED_EDGE('',*,*,#3550,.T.);
#4954=ORIENTED_EDGE('',*,*,#3548,.T.);
#4955=ORIENTED_EDGE('',*,*,#3550,.F.);
#4956=ORIENTED_EDGE('',*,*,#3551,.F.);
#4957=ORIENTED_EDGE('',*,*,#3552,.T.);
#4958=ORIENTED_EDGE('',*,*,#3549,.T.);
#4959=ORIENTED_EDGE('',*,*,#3552,.F.);
#4960=ORIENTED_EDGE('',*,*,#3553,.F.);
#4961=ORIENTED_EDGE('',*,*,#3554,.T.);
#4962=ORIENTED_EDGE('',*,*,#3551,.T.);
#4963=ORIENTED_EDGE('',*,*,#3554,.F.);
#4964=ORIENTED_EDGE('',*,*,#3553,.T.);
#4965=ORIENTED_EDGE('',*,*,#3555,.F.);
#4966=ORIENTED_EDGE('',*,*,#3556,.F.);
#4967=ORIENTED_EDGE('',*,*,#3557,.T.);
#4968=ORIENTED_EDGE('',*,*,#3555,.T.);
#4969=ORIENTED_EDGE('',*,*,#3557,.F.);
#4970=ORIENTED_EDGE('',*,*,#3558,.F.);
#4971=ORIENTED_EDGE('',*,*,#3559,.T.);
#4972=ORIENTED_EDGE('',*,*,#3556,.T.);
#4973=ORIENTED_EDGE('',*,*,#3559,.F.);
#4974=ORIENTED_EDGE('',*,*,#3560,.F.);
#4975=ORIENTED_EDGE('',*,*,#3561,.T.);
#4976=ORIENTED_EDGE('',*,*,#3558,.T.);
#4977=ORIENTED_EDGE('',*,*,#3561,.F.);
#4978=ORIENTED_EDGE('',*,*,#3560,.T.);
#4979=ORIENTED_EDGE('',*,*,#3562,.T.);
#4980=ORIENTED_EDGE('',*,*,#3563,.T.);
#4981=ORIENTED_EDGE('',*,*,#3564,.T.);
#4982=ORIENTED_EDGE('',*,*,#3565,.F.);
#4983=ORIENTED_EDGE('',*,*,#3566,.T.);
#4984=ORIENTED_EDGE('',*,*,#3567,.T.);
#4985=ORIENTED_EDGE('',*,*,#3568,.T.);
#4986=ORIENTED_EDGE('',*,*,#3563,.F.);
#4987=ORIENTED_EDGE('',*,*,#3569,.T.);
#4988=ORIENTED_EDGE('',*,*,#3570,.T.);
#4989=ORIENTED_EDGE('',*,*,#3571,.T.);
#4990=ORIENTED_EDGE('',*,*,#3567,.F.);
#4991=ORIENTED_EDGE('',*,*,#3572,.T.);
#4992=ORIENTED_EDGE('',*,*,#3573,.T.);
#4993=ORIENTED_EDGE('',*,*,#3574,.T.);
#4994=ORIENTED_EDGE('',*,*,#3570,.F.);
#4995=ORIENTED_EDGE('',*,*,#3575,.T.);
#4996=ORIENTED_EDGE('',*,*,#3576,.T.);
#4997=ORIENTED_EDGE('',*,*,#3577,.T.);
#4998=ORIENTED_EDGE('',*,*,#3573,.F.);
#4999=ORIENTED_EDGE('',*,*,#3578,.T.);
#5000=ORIENTED_EDGE('',*,*,#3565,.T.);
#5001=ORIENTED_EDGE('',*,*,#3579,.T.);
#5002=ORIENTED_EDGE('',*,*,#3576,.F.);
#5003=ORIENTED_EDGE('',*,*,#3578,.F.);
#5004=ORIENTED_EDGE('',*,*,#3575,.F.);
#5005=ORIENTED_EDGE('',*,*,#3572,.F.);
#5006=ORIENTED_EDGE('',*,*,#3569,.F.);
#5007=ORIENTED_EDGE('',*,*,#3566,.F.);
#5008=ORIENTED_EDGE('',*,*,#3562,.F.);
#5009=ORIENTED_EDGE('',*,*,#3579,.F.);
#5010=ORIENTED_EDGE('',*,*,#3564,.F.);
#5011=ORIENTED_EDGE('',*,*,#3568,.F.);
#5012=ORIENTED_EDGE('',*,*,#3571,.F.);
#5013=ORIENTED_EDGE('',*,*,#3574,.F.);
#5014=ORIENTED_EDGE('',*,*,#3577,.F.);
#5256=CYLINDRICAL_SURFACE('',#6489,0.425);
#5257=CYLINDRICAL_SURFACE('',#6497,0.24505);
#5534=ADVANCED_FACE('',(#863),#558,.T.);
#5535=ADVANCED_FACE('',(#864),#14,.T.);
#5536=ADVANCED_FACE('',(#865),#5256,.T.);
#5537=ADVANCED_FACE('',(#866),#15,.T.);
#5538=ADVANCED_FACE('',(#867,#429),#559,.T.);
#5539=ADVANCED_FACE('',(#868),#16,.T.);
#5540=ADVANCED_FACE('',(#869),#5257,.T.);
#5541=ADVANCED_FACE('',(#870),#17,.T.);
#5542=ADVANCED_FACE('',(#871),#560,.T.);
#5543=ADVANCED_FACE('',(#872),#561,.F.);
#5544=ADVANCED_FACE('',(#873),#562,.F.);
#5545=ADVANCED_FACE('',(#874),#563,.F.);
#5546=ADVANCED_FACE('',(#875),#564,.F.);
#5547=ADVANCED_FACE('',(#876),#565,.F.);
#5548=ADVANCED_FACE('',(#877),#566,.F.);
#5549=ADVANCED_FACE('',(#878),#567,.F.);
#5550=ADVANCED_FACE('',(#879),#568,.F.);
#5597=CLOSED_SHELL('',(#5534,#5535,#5536,#5537,#5538,#5539,#5540,#5541,
#5542));
#5598=CLOSED_SHELL('',(#5543,#5544,#5545,#5546,#5547,#5548,#5549,#5550));
#6484=AXIS2_PLACEMENT_3D('',#10566,#8093,#8094);
#6485=AXIS2_PLACEMENT_3D('',#10567,#8095,#8096);
#6486=AXIS2_PLACEMENT_3D('',#10569,#8097,#8098);
#6487=AXIS2_PLACEMENT_3D('',#10570,#8099,#8100);
#6488=AXIS2_PLACEMENT_3D('',#10572,#8101,#8102);
#6489=AXIS2_PLACEMENT_3D('',#10574,#8104,#8105);
#6490=AXIS2_PLACEMENT_3D('',#10576,#8106,#8107);
#6491=AXIS2_PLACEMENT_3D('',#10578,#8109,#8110);
#6492=AXIS2_PLACEMENT_3D('',#10580,#8111,#8112);
#6493=AXIS2_PLACEMENT_3D('',#10582,#8114,#8115);
#6494=AXIS2_PLACEMENT_3D('',#10584,#8116,#8117);
#6495=AXIS2_PLACEMENT_3D('',#10585,#8118,#8119);
#6496=AXIS2_PLACEMENT_3D('',#10587,#8120,#8121);
#6497=AXIS2_PLACEMENT_3D('',#10589,#8123,#8124);
#6498=AXIS2_PLACEMENT_3D('',#10591,#8125,#8126);
#6499=AXIS2_PLACEMENT_3D('',#10593,#8128,#8129);
#6500=AXIS2_PLACEMENT_3D('',#10595,#8130,#8131);
#6501=AXIS2_PLACEMENT_3D('',#10597,#8133,#8134);
#6502=AXIS2_PLACEMENT_3D('',#10598,#8135,#8136);
#6503=AXIS2_PLACEMENT_3D('',#10607,#8141,#8142);
#6504=AXIS2_PLACEMENT_3D('',#10613,#8146,#8147);
#6505=AXIS2_PLACEMENT_3D('',#10619,#8151,#8152);
#6506=AXIS2_PLACEMENT_3D('',#10625,#8156,#8157);
#6507=AXIS2_PLACEMENT_3D('',#10631,#8161,#8162);
#6508=AXIS2_PLACEMENT_3D('',#10634,#8165,#8166);
#6509=AXIS2_PLACEMENT_3D('',#10635,#8167,#8168);
#8093=DIRECTION('axis',(0.,0.,1.));
#8094=DIRECTION('refdir',(1.,0.,0.));
#8095=DIRECTION('center_axis',(0.,1.,0.));
#8096=DIRECTION('ref_axis',(0.,0.,1.));
#8097=DIRECTION('center_axis',(0.,-1.,0.));
#8098=DIRECTION('ref_axis',(1.,0.,0.));
#8099=DIRECTION('center_axis',(0.,-1.,0.));
#8100=DIRECTION('ref_axis',(1.,0.,0.));
#8101=DIRECTION('center_axis',(0.,-1.,0.));
#8102=DIRECTION('ref_axis',(1.,0.,0.));
#8103=DIRECTION('',(0.707106781186548,0.707106781186547,8.65956056235493E-17));
#8104=DIRECTION('center_axis',(0.,-1.,0.));
#8105=DIRECTION('ref_axis',(1.,0.,0.));
#8106=DIRECTION('center_axis',(0.,-1.,0.));
#8107=DIRECTION('ref_axis',(1.,0.,0.));
#8108=DIRECTION('',(0.,1.,0.));
#8109=DIRECTION('center_axis',(0.,1.,0.));
#8110=DIRECTION('ref_axis',(1.,0.,0.));
#8111=DIRECTION('center_axis',(0.,-1.,0.));
#8112=DIRECTION('ref_axis',(1.,0.,0.));
#8113=DIRECTION('',(-0.707106781186547,0.707106781186548,-8.65956056235493E-17));
#8114=DIRECTION('center_axis',(0.,-1.,0.));
#8115=DIRECTION('ref_axis',(0.,0.,-1.));
#8116=DIRECTION('center_axis',(0.,-1.,0.));
#8117=DIRECTION('ref_axis',(1.,0.,0.));
#8118=DIRECTION('center_axis',(0.,1.,0.));
#8119=DIRECTION('ref_axis',(1.,0.,0.));
#8120=DIRECTION('center_axis',(0.,1.,0.));
#8121=DIRECTION('ref_axis',(1.,0.,0.));
#8122=DIRECTION('',(-0.447213595499958,0.894427190999916,-5.47678698264203E-17));
#8123=DIRECTION('center_axis',(0.,-1.,0.));
#8124=DIRECTION('ref_axis',(1.,0.,0.));
#8125=DIRECTION('center_axis',(0.,1.,0.));
#8126=DIRECTION('ref_axis',(1.,0.,0.));
#8127=DIRECTION('',(0.,1.,0.));
#8128=DIRECTION('center_axis',(0.,1.,0.));
#8129=DIRECTION('ref_axis',(1.,0.,0.));
#8130=DIRECTION('center_axis',(0.,-1.,0.));
#8131=DIRECTION('ref_axis',(1.,0.,0.));
#8132=DIRECTION('',(-0.707106781186547,0.707106781186548,-8.65956056235493E-17));
#8133=DIRECTION('center_axis',(0.,-1.,0.));
#8134=DIRECTION('ref_axis',(0.,0.,-1.));
#8135=DIRECTION('center_axis',(0.866025403784439,0.,-0.5));
#8136=DIRECTION('ref_axis',(0.5,0.,0.866025403784439));
#8137=DIRECTION('',(-0.5,0.,-0.866025403784439));
#8138=DIRECTION('',(0.,-1.,0.));
#8139=DIRECTION('',(0.5,0.,0.866025403784439));
#8140=DIRECTION('',(0.,-1.,0.));
#8141=DIRECTION('center_axis',(1.20185167898973E-16,0.,-1.));
#8142=DIRECTION('ref_axis',(1.,0.,1.20185167898973E-16));
#8143=DIRECTION('',(-1.,0.,-1.20185167898973E-16));
#8144=DIRECTION('',(0.,-1.,0.));
#8145=DIRECTION('',(1.,0.,1.20185167898973E-16));
#8146=DIRECTION('center_axis',(-0.866025403784439,0.,-0.5));
#8147=DIRECTION('ref_axis',(0.5,0.,-0.866025403784439));
#8148=DIRECTION('',(-0.5,0.,0.866025403784439));
#8149=DIRECTION('',(0.,-1.,0.));
#8150=DIRECTION('',(0.5,0.,-0.866025403784439));
#8151=DIRECTION('center_axis',(-0.866025403784439,0.,0.5));
#8152=DIRECTION('ref_axis',(-0.5,0.,-0.866025403784439));
#8153=DIRECTION('',(0.5,0.,0.866025403784439));
#8154=DIRECTION('',(0.,-1.,0.));
#8155=DIRECTION('',(-0.5,0.,-0.866025403784439));
#8156=DIRECTION('center_axis',(-2.40370335797945E-16,0.,1.));
#8157=DIRECTION('ref_axis',(-1.,0.,-2.40370335797945E-16));
#8158=DIRECTION('',(1.,0.,2.40370335797945E-16));
#8159=DIRECTION('',(0.,-1.,0.));
#8160=DIRECTION('',(-1.,0.,-2.40370335797945E-16));
#8161=DIRECTION('center_axis',(0.866025403784439,0.,0.5));
#8162=DIRECTION('ref_axis',(-0.5,0.,0.866025403784439));
#8163=DIRECTION('',(0.5,0.,-0.866025403784439));
#8164=DIRECTION('',(-0.5,0.,0.866025403784439));
#8165=DIRECTION('center_axis',(0.,1.,0.));
#8166=DIRECTION('ref_axis',(1.,0.,0.));
#8167=DIRECTION('center_axis',(0.,-1.,0.));
#8168=DIRECTION('ref_axis',(0.,0.,-1.));
#10566=CARTESIAN_POINT('',(0.,0.,0.));
#10567=CARTESIAN_POINT('Origin',(0.375,0.5,0.));
#10568=CARTESIAN_POINT('',(-0.375,0.5,-4.59242549680257E-17));
#10569=CARTESIAN_POINT('Origin',(0.,0.5,0.));
#10570=CARTESIAN_POINT('Origin',(0.,0.475,0.));
#10571=CARTESIAN_POINT('',(-0.425,0.45,-5.20474889637625E-17));
#10572=CARTESIAN_POINT('Origin',(0.,0.45,0.));
#10573=CARTESIAN_POINT('',(-0.4,0.475,-4.89858719658941E-17));
#10574=CARTESIAN_POINT('Origin',(0.,0.24,0.));
#10575=CARTESIAN_POINT('',(-0.425,0.0299999999999998,-5.20474889637625E-17));
#10576=CARTESIAN_POINT('Origin',(0.,0.0299999999999998,0.));
#10577=CARTESIAN_POINT('',(-0.425,0.24,-5.20474889637625E-17));
#10578=CARTESIAN_POINT('Origin',(0.,0.0150000000000001,0.));
#10579=CARTESIAN_POINT('',(-0.395,4.85722573273506E-17,-4.83735485663204E-17));
#10580=CARTESIAN_POINT('Origin',(0.,0.,0.));
#10581=CARTESIAN_POINT('',(-0.41,0.0150000000000001,-5.02105187650415E-17));
#10582=CARTESIAN_POINT('Origin',(0.27,0.,0.));
#10583=CARTESIAN_POINT('',(-0.27,0.,-3.30654635769785E-17));
#10584=CARTESIAN_POINT('Origin',(0.,0.,0.));
#10585=CARTESIAN_POINT('Origin',(0.,-0.02,0.));
#10586=CARTESIAN_POINT('',(-0.24505,-0.0498999999999999,3.00099698131059E-17));
#10587=CARTESIAN_POINT('Origin',(0.,-0.0498999999999999,0.));
#10588=CARTESIAN_POINT('',(-0.26,-0.02,-3.18408167778312E-17));
#10589=CARTESIAN_POINT('Origin',(0.,-0.995,0.));
#10590=CARTESIAN_POINT('',(-0.24505,-1.95495,3.00099698131059E-17));
#10591=CARTESIAN_POINT('Origin',(0.,-1.95495,0.));
#10592=CARTESIAN_POINT('',(-0.24505,-0.995,-3.00099698131059E-17));
#10593=CARTESIAN_POINT('Origin',(0.,-1.975,0.));
#10594=CARTESIAN_POINT('',(-0.2,-2.,-2.44929359829471E-17));
#10595=CARTESIAN_POINT('Origin',(0.,-2.,0.));
#10596=CARTESIAN_POINT('',(-0.225,-1.975,-2.75545529808154E-17));
#10597=CARTESIAN_POINT('Origin',(0.,-2.,0.));
#10598=CARTESIAN_POINT('Origin',(0.115470053837925,-0.5,-0.2));
#10599=CARTESIAN_POINT('',(0.23094010767585,-0.5,0.));
#10600=CARTESIAN_POINT('',(0.115470053837925,-0.5,-0.2));
#10601=CARTESIAN_POINT('',(0.23094010767585,-0.5,0.));
#10602=CARTESIAN_POINT('',(0.115470053837925,-0.8,-0.2));
#10603=CARTESIAN_POINT('',(0.115470053837925,-0.5,-0.2));
#10604=CARTESIAN_POINT('',(0.23094010767585,-0.8,0.));
#10605=CARTESIAN_POINT('',(0.23094010767585,-0.8,0.));
#10606=CARTESIAN_POINT('',(0.23094010767585,-0.5,0.));
#10607=CARTESIAN_POINT('Origin',(-0.115470053837925,-0.5,-0.2));
#10608=CARTESIAN_POINT('',(-0.115470053837925,-0.5,-0.2));
#10609=CARTESIAN_POINT('',(0.115470053837925,-0.5,-0.2));
#10610=CARTESIAN_POINT('',(-0.115470053837925,-0.8,-0.2));
#10611=CARTESIAN_POINT('',(-0.115470053837925,-0.5,-0.2));
#10612=CARTESIAN_POINT('',(0.115470053837925,-0.8,-0.2));
#10613=CARTESIAN_POINT('Origin',(-0.23094010767585,-0.5,-2.77555756156289E-17));
#10614=CARTESIAN_POINT('',(-0.23094010767585,-0.5,-2.82820063659975E-17));
#10615=CARTESIAN_POINT('',(-0.115470053837925,-0.5,-0.2));
#10616=CARTESIAN_POINT('',(-0.23094010767585,-0.8,-2.77555756156289E-17));
#10617=CARTESIAN_POINT('',(-0.23094010767585,-0.5,-2.82820063659975E-17));
#10618=CARTESIAN_POINT('',(-0.115470053837925,-0.8,-0.2));
#10619=CARTESIAN_POINT('Origin',(-0.115470053837925,-0.5,0.2));
#10620=CARTESIAN_POINT('',(-0.115470053837925,-0.5,0.2));
#10621=CARTESIAN_POINT('',(-0.23094010767585,-0.5,-2.82820063659975E-17));
#10622=CARTESIAN_POINT('',(-0.115470053837925,-0.8,0.2));
#10623=CARTESIAN_POINT('',(-0.115470053837925,-0.5,0.2));
#10624=CARTESIAN_POINT('',(-0.23094010767585,-0.8,-2.82820063659975E-17));
#10625=CARTESIAN_POINT('Origin',(0.115470053837925,-0.5,0.2));
#10626=CARTESIAN_POINT('',(0.115470053837925,-0.5,0.2));
#10627=CARTESIAN_POINT('',(-0.115470053837925,-0.5,0.2));
#10628=CARTESIAN_POINT('',(0.115470053837925,-0.8,0.2));
#10629=CARTESIAN_POINT('',(0.115470053837925,-0.5,0.2));
#10630=CARTESIAN_POINT('',(-0.115470053837925,-0.8,0.2));
#10631=CARTESIAN_POINT('Origin',(0.23094010767585,-0.5,0.));
#10632=CARTESIAN_POINT('',(0.115470053837925,-0.5,0.2));
#10633=CARTESIAN_POINT('',(0.115470053837925,-0.8,0.2));
#10634=CARTESIAN_POINT('Origin',(0.,-0.5,0.));
#10635=CARTESIAN_POINT('Origin',(0.,-0.8,0.));
#10788=UNCERTAINTY_MEASURE_WITH_UNIT(LENGTH_MEASURE(0.001),#10822,
'DISTANCE_ACCURACY_VALUE',
'Maximum model space distance between geometric entities at asserted c
onnectivities');
#10791=UNCERTAINTY_MEASURE_WITH_UNIT(LENGTH_MEASURE(0.001),#10822,
'DISTANCE_ACCURACY_VALUE',
'Maximum model space distance between geometric entities at asserted c
onnectivities');
#10818=(
GEOMETRIC_REPRESENTATION_CONTEXT(3)
GLOBAL_UNCERTAINTY_ASSIGNED_CONTEXT((#10788))
GLOBAL_UNIT_ASSIGNED_CONTEXT((#10822,#10824,#10825))
REPRESENTATION_CONTEXT('','3D')
);
#10821=(
GEOMETRIC_REPRESENTATION_CONTEXT(3)
GLOBAL_UNCERTAINTY_ASSIGNED_CONTEXT((#10791))
GLOBAL_UNIT_ASSIGNED_CONTEXT((#10822,#10824,#10825))
REPRESENTATION_CONTEXT('','3D')
);
#10822=(
LENGTH_UNIT()
NAMED_UNIT(*)
SI_UNIT(.CENTI.,.METRE.)
);
#10824=(
NAMED_UNIT(*)
PLANE_ANGLE_UNIT()
SI_UNIT($,.RADIAN.)
);
#10825=(
NAMED_UNIT(*)
SI_UNIT($,.STERADIAN.)
SOLID_ANGLE_UNIT()
);
#10852=SHAPE_DEFINITION_REPRESENTATION(#10900,#10950);
#10900=PRODUCT_DEFINITION_SHAPE('',$,#10980);
#10950=SHAPE_REPRESENTATION('',(#6484),#10818);
#10953=PRODUCT_DEFINITION_CONTEXT('part definition',#11042,'design');
#10980=PRODUCT_DEFINITION('Cap Screw - M5x20','Cap Screw - M5x20',#11009,
#10953);
#11009=PRODUCT_DEFINITION_FORMATION('',$,#11070);
#11042=APPLICATION_CONTEXT(
'Core Data for Automotive Mechanical Design Process');
#11043=PRODUCT_CONTEXT('part definition',#11042,'mechanical');
#11070=PRODUCT('Cap Screw - M5x20','Cap Screw - M5x20',
'Cap Screw - M5x20',(#11043));
#11136=COLOUR_RGB('Black',0.12,0.14,0.17);
#11137=FILL_AREA_STYLE_COLOUR('',#11136);
#11138=FILL_AREA_STYLE('',(#11137));
#11139=SURFACE_STYLE_FILL_AREA(#11138);
#11140=SURFACE_SIDE_STYLE('',(#11139));
#11141=SURFACE_STYLE_USAGE(.BOTH.,#11140);
#11142=PRESENTATION_STYLE_ASSIGNMENT((#11141));
ENDSEC;
END-ISO-10303-21;
